ISO-10303-21;
HEADER;
/* Generated by software containing ST-Developer
 * from STEP Tools, Inc. (www.steptools.com) 
 */

FILE_DESCRIPTION(
/* description */ ('Bin tilter linkage'),
/* implementation_level */ '2;1');

FILE_NAME(
/* name */ 'Screw bearing keeper (2).step',
/* time_stamp */ '2026-10-28T03:26:24-07:00',
/* author */ (''),
/* organization */ (''),
/* preprocessor_version */ 'ST-DEVELOPER v20.2',
/* originating_system */ 'Autodesk Translation Framework v15.17.0.0',
/* authorisation */ '');

FILE_SCHEMA (('AUTOMOTIVE_DESIGN { 1 0 10303 214 3 1 1 }'));
ENDSEC;

DATA;
#10=MECHANICAL_DESIGN_GEOMETRIC_PRESENTATION_REPRESENTATION('',(#883),#23728);
#671=SHAPE_REPRESENTATION_RELATIONSHIP('SRR','None',#24135,#777);
#777=ADVANCED_BREP_SHAPE_REPRESENTATION('',(#997),#23635);
#883=STYLED_ITEM('',(#24772),#997);
#997=MANIFOLD_SOLID_BREP('Body1',#12413);
#1217=FACE_BOUND('',#2990,.T.);
#1218=FACE_BOUND('',#2991,.T.);
#1219=FACE_BOUND('',#2992,.T.);
#1220=FACE_BOUND('',#2997,.T.);
#1221=FACE_BOUND('',#2998,.T.);
#1222=FACE_BOUND('',#2999,.T.);
#1586=PLANE('',#14088);
#1587=PLANE('',#14098);
#2078=FACE_OUTER_BOUND('',#2985,.T.);
#2079=FACE_OUTER_BOUND('',#2986,.T.);
#2080=FACE_OUTER_BOUND('',#2987,.T.);
#2081=FACE_OUTER_BOUND('',#2988,.T.);
#2082=FACE_OUTER_BOUND('',#2989,.T.);
#2083=FACE_OUTER_BOUND('',#2993,.T.);
#2084=FACE_OUTER_BOUND('',#2994,.T.);
#2085=FACE_OUTER_BOUND('',#2995,.T.);
#2086=FACE_OUTER_BOUND('',#2996,.T.);
#2985=EDGE_LOOP('',(#9165,#9166,#9167,#9168));
#2986=EDGE_LOOP('',(#9169,#9170,#9171,#9172));
#2987=EDGE_LOOP('',(#9173,#9174,#9175,#9176));
#2988=EDGE_LOOP('',(#9177,#9178,#9179,#9180));
#2989=EDGE_LOOP('',(#9181,#9182,#9183,#9184));
#2990=EDGE_LOOP('',(#9185));
#2991=EDGE_LOOP('',(#9186));
#2992=EDGE_LOOP('',(#9187));
#2993=EDGE_LOOP('',(#9188,#9189,#9190,#9191));
#2994=EDGE_LOOP('',(#9192,#9193,#9194,#9195));
#2995=EDGE_LOOP('',(#9196,#9197,#9198,#9199));
#2996=EDGE_LOOP('',(#9200,#9201,#9202,#9203));
#2997=EDGE_LOOP('',(#9204));
#2998=EDGE_LOOP('',(#9205));
#2999=EDGE_LOOP('',(#9206));
#4057=LINE('',#20621,#4732);
#4058=LINE('',#20627,#4733);
#4059=LINE('',#20632,#4734);
#4060=LINE('',#20636,#4735);
#4061=LINE('',#20641,#4736);
#4062=LINE('',#20645,#4737);
#4063=LINE('',#20658,#4738);
#4732=VECTOR('',#16486,0.225);
#4733=VECTOR('',#16493,0.225);
#4734=VECTOR('',#16498,1.);
#4735=VECTOR('',#16501,1.);
#4736=VECTOR('',#16506,1.);
#4737=VECTOR('',#16509,1.);
#4738=VECTOR('',#16530,1.02);
#5387=CIRCLE('',#14077,0.225);
#5388=CIRCLE('',#14078,0.225);
#5389=CIRCLE('',#14080,0.225);
#5390=CIRCLE('',#14081,0.225);
#5391=CIRCLE('',#14083,0.61);
#5392=CIRCLE('',#14084,0.61);
#5393=CIRCLE('',#14086,0.61);
#5394=CIRCLE('',#14087,0.61);
#5395=CIRCLE('',#14089,2.1);
#5396=CIRCLE('',#14090,2.1);
#5397=CIRCLE('',#14091,1.02);
#5398=CIRCLE('',#14093,2.1);
#5399=CIRCLE('',#14095,2.1);
#5400=CIRCLE('',#14097,1.02);
#6221=VERTEX_POINT('',#20618);
#6222=VERTEX_POINT('',#20620);
#6223=VERTEX_POINT('',#20624);
#6224=VERTEX_POINT('',#20626);
#6225=VERTEX_POINT('',#20630);
#6226=VERTEX_POINT('',#20631);
#6227=VERTEX_POINT('',#20633);
#6228=VERTEX_POINT('',#20635);
#6229=VERTEX_POINT('',#20639);
#6230=VERTEX_POINT('',#20640);
#6231=VERTEX_POINT('',#20642);
#6232=VERTEX_POINT('',#20644);
#6233=VERTEX_POINT('',#20650);
#6234=VERTEX_POINT('',#20657);
#7322=EDGE_CURVE('',#6221,#6221,#5387,.T.);
#7323=EDGE_CURVE('',#6221,#6222,#4057,.T.);
#7324=EDGE_CURVE('',#6222,#6222,#5388,.T.);
#7325=EDGE_CURVE('',#6223,#6223,#5389,.T.);
#7326=EDGE_CURVE('',#6223,#6224,#4058,.T.);
#7327=EDGE_CURVE('',#6224,#6224,#5390,.T.);
#7328=EDGE_CURVE('',#6225,#6226,#4059,.T.);
#7329=EDGE_CURVE('',#6227,#6225,#5391,.T.);
#7330=EDGE_CURVE('',#6228,#6227,#4060,.T.);
#7331=EDGE_CURVE('',#6226,#6228,#5392,.T.);
#7332=EDGE_CURVE('',#6229,#6230,#4061,.T.);
#7333=EDGE_CURVE('',#6231,#6229,#5393,.T.);
#7334=EDGE_CURVE('',#6232,#6231,#4062,.T.);
#7335=EDGE_CURVE('',#6230,#6232,#5394,.T.);
#7336=EDGE_CURVE('',#6225,#6231,#5395,.T.);
#7337=EDGE_CURVE('',#6229,#6227,#5396,.T.);
#7338=EDGE_CURVE('',#6233,#6233,#5397,.T.);
#7339=EDGE_CURVE('',#6226,#6232,#5398,.T.);
#7340=EDGE_CURVE('',#6230,#6228,#5399,.T.);
#7341=EDGE_CURVE('',#6233,#6234,#4063,.T.);
#7342=EDGE_CURVE('',#6234,#6234,#5400,.T.);
#9165=ORIENTED_EDGE('',*,*,#7322,.F.);
#9166=ORIENTED_EDGE('',*,*,#7323,.T.);
#9167=ORIENTED_EDGE('',*,*,#7324,.F.);
#9168=ORIENTED_EDGE('',*,*,#7323,.F.);
#9169=ORIENTED_EDGE('',*,*,#7325,.F.);
#9170=ORIENTED_EDGE('',*,*,#7326,.T.);
#9171=ORIENTED_EDGE('',*,*,#7327,.F.);
#9172=ORIENTED_EDGE('',*,*,#7326,.F.);
#9173=ORIENTED_EDGE('',*,*,#7328,.F.);
#9174=ORIENTED_EDGE('',*,*,#7329,.F.);
#9175=ORIENTED_EDGE('',*,*,#7330,.F.);
#9176=ORIENTED_EDGE('',*,*,#7331,.F.);
#9177=ORIENTED_EDGE('',*,*,#7332,.F.);
#9178=ORIENTED_EDGE('',*,*,#7333,.F.);
#9179=ORIENTED_EDGE('',*,*,#7334,.F.);
#9180=ORIENTED_EDGE('',*,*,#7335,.F.);
#9181=ORIENTED_EDGE('',*,*,#7329,.T.);
#9182=ORIENTED_EDGE('',*,*,#7336,.T.);
#9183=ORIENTED_EDGE('',*,*,#7333,.T.);
#9184=ORIENTED_EDGE('',*,*,#7337,.T.);
#9185=ORIENTED_EDGE('',*,*,#7324,.T.);
#9186=ORIENTED_EDGE('',*,*,#7327,.T.);
#9187=ORIENTED_EDGE('',*,*,#7338,.T.);
#9188=ORIENTED_EDGE('',*,*,#7328,.T.);
#9189=ORIENTED_EDGE('',*,*,#7339,.T.);
#9190=ORIENTED_EDGE('',*,*,#7334,.T.);
#9191=ORIENTED_EDGE('',*,*,#7336,.F.);
#9192=ORIENTED_EDGE('',*,*,#7330,.T.);
#9193=ORIENTED_EDGE('',*,*,#7337,.F.);
#9194=ORIENTED_EDGE('',*,*,#7332,.T.);
#9195=ORIENTED_EDGE('',*,*,#7340,.T.);
#9196=ORIENTED_EDGE('',*,*,#7338,.F.);
#9197=ORIENTED_EDGE('',*,*,#7341,.T.);
#9198=ORIENTED_EDGE('',*,*,#7342,.T.);
#9199=ORIENTED_EDGE('',*,*,#7341,.F.);
#9200=ORIENTED_EDGE('',*,*,#7331,.T.);
#9201=ORIENTED_EDGE('',*,*,#7340,.F.);
#9202=ORIENTED_EDGE('',*,*,#7335,.T.);
#9203=ORIENTED_EDGE('',*,*,#7339,.F.);
#9204=ORIENTED_EDGE('',*,*,#7322,.T.);
#9205=ORIENTED_EDGE('',*,*,#7325,.T.);
#9206=ORIENTED_EDGE('',*,*,#7342,.F.);
#11361=CYLINDRICAL_SURFACE('',#14076,0.225);
#11362=CYLINDRICAL_SURFACE('',#14079,0.225);
#11363=CYLINDRICAL_SURFACE('',#14082,0.61);
#11364=CYLINDRICAL_SURFACE('',#14085,0.61);
#11365=CYLINDRICAL_SURFACE('',#14092,2.1);
#11366=CYLINDRICAL_SURFACE('',#14094,2.1);
#11367=CYLINDRICAL_SURFACE('',#14096,1.02);
#11803=ADVANCED_FACE('',(#2078),#11361,.F.);
#11804=ADVANCED_FACE('',(#2079),#11362,.F.);
#11805=ADVANCED_FACE('',(#2080),#11363,.F.);
#11806=ADVANCED_FACE('',(#2081),#11364,.F.);
#11807=ADVANCED_FACE('',(#2082,#1217,#1218,#1219),#1586,.T.);
#11808=ADVANCED_FACE('',(#2083),#11365,.T.);
#11809=ADVANCED_FACE('',(#2084),#11366,.T.);
#11810=ADVANCED_FACE('',(#2085),#11367,.F.);
#11811=ADVANCED_FACE('',(#2086,#1220,#1221,#1222),#1587,.F.);
#12413=CLOSED_SHELL('',(#11803,#11804,#11805,#11806,#11807,#11808,#11809,
#11810,#11811));
#14075=AXIS2_PLACEMENT_3D('',#20616,#16480,#16481);
#14076=AXIS2_PLACEMENT_3D('',#20617,#16482,#16483);
#14077=AXIS2_PLACEMENT_3D('',#20619,#16484,#16485);
#14078=AXIS2_PLACEMENT_3D('',#20622,#16487,#16488);
#14079=AXIS2_PLACEMENT_3D('',#20623,#16489,#16490);
#14080=AXIS2_PLACEMENT_3D('',#20625,#16491,#16492);
#14081=AXIS2_PLACEMENT_3D('',#20628,#16494,#16495);
#14082=AXIS2_PLACEMENT_3D('',#20629,#16496,#16497);
#14083=AXIS2_PLACEMENT_3D('',#20634,#16499,#16500);
#14084=AXIS2_PLACEMENT_3D('',#20637,#16502,#16503);
#14085=AXIS2_PLACEMENT_3D('',#20638,#16504,#16505);
#14086=AXIS2_PLACEMENT_3D('',#20643,#16507,#16508);
#14087=AXIS2_PLACEMENT_3D('',#20646,#16510,#16511);
#14088=AXIS2_PLACEMENT_3D('',#20647,#16512,#16513);
#14089=AXIS2_PLACEMENT_3D('',#20648,#16514,#16515);
#14090=AXIS2_PLACEMENT_3D('',#20649,#16516,#16517);
#14091=AXIS2_PLACEMENT_3D('',#20651,#16518,#16519);
#14092=AXIS2_PLACEMENT_3D('',#20652,#16520,#16521);
#14093=AXIS2_PLACEMENT_3D('',#20653,#16522,#16523);
#14094=AXIS2_PLACEMENT_3D('',#20654,#16524,#16525);
#14095=AXIS2_PLACEMENT_3D('',#20655,#16526,#16527);
#14096=AXIS2_PLACEMENT_3D('',#20656,#16528,#16529);
#14097=AXIS2_PLACEMENT_3D('',#20659,#16531,#16532);
#14098=AXIS2_PLACEMENT_3D('',#20660,#16533,#16534);
#16480=DIRECTION('axis',(0.,0.,1.));
#16481=DIRECTION('refdir',(1.,0.,0.));
#16482=DIRECTION('center_axis',(1.,0.,0.));
#16483=DIRECTION('ref_axis',(0.,0.,-1.));
#16484=DIRECTION('center_axis',(1.,0.,0.));
#16485=DIRECTION('ref_axis',(0.,0.,-1.));
#16486=DIRECTION('',(1.,0.,0.));
#16487=DIRECTION('center_axis',(-1.,0.,0.));
#16488=DIRECTION('ref_axis',(0.,0.,-1.));
#16489=DIRECTION('center_axis',(1.,0.,0.));
#16490=DIRECTION('ref_axis',(0.,0.,-1.));
#16491=DIRECTION('center_axis',(1.,0.,0.));
#16492=DIRECTION('ref_axis',(0.,0.,-1.));
#16493=DIRECTION('',(1.,0.,0.));
#16494=DIRECTION('center_axis',(-1.,0.,0.));
#16495=DIRECTION('ref_axis',(0.,0.,-1.));
#16496=DIRECTION('center_axis',(1.,0.,0.));
#16497=DIRECTION('ref_axis',(0.,0.,-1.));
#16498=DIRECTION('',(-1.,0.,0.));
#16499=DIRECTION('center_axis',(-1.,0.,0.));
#16500=DIRECTION('ref_axis',(0.,0.,-1.));
#16501=DIRECTION('',(1.,0.,0.));
#16502=DIRECTION('center_axis',(1.,0.,0.));
#16503=DIRECTION('ref_axis',(0.,0.,-1.));
#16504=DIRECTION('center_axis',(1.,0.,0.));
#16505=DIRECTION('ref_axis',(0.,0.,-1.));
#16506=DIRECTION('',(-1.,0.,0.));
#16507=DIRECTION('center_axis',(-1.,0.,0.));
#16508=DIRECTION('ref_axis',(0.,0.,-1.));
#16509=DIRECTION('',(1.,0.,0.));
#16510=DIRECTION('center_axis',(1.,0.,0.));
#16511=DIRECTION('ref_axis',(0.,0.,-1.));
#16512=DIRECTION('center_axis',(1.,0.,0.));
#16513=DIRECTION('ref_axis',(0.,0.,-1.));
#16514=DIRECTION('center_axis',(1.,0.,0.));
#16515=DIRECTION('ref_axis',(0.,0.,-1.));
#16516=DIRECTION('center_axis',(1.,0.,0.));
#16517=DIRECTION('ref_axis',(0.,0.,-1.));
#16518=DIRECTION('center_axis',(-1.,0.,0.));
#16519=DIRECTION('ref_axis',(0.,0.,-1.));
#16520=DIRECTION('center_axis',(1.,0.,0.));
#16521=DIRECTION('ref_axis',(0.,0.,-1.));
#16522=DIRECTION('center_axis',(1.,0.,0.));
#16523=DIRECTION('ref_axis',(0.,0.,-1.));
#16524=DIRECTION('center_axis',(1.,0.,0.));
#16525=DIRECTION('ref_axis',(0.,-1.22464679914735E-16,1.));
#16526=DIRECTION('center_axis',(1.,0.,0.));
#16527=DIRECTION('ref_axis',(0.,0.,-1.));
#16528=DIRECTION('center_axis',(1.,0.,0.));
#16529=DIRECTION('ref_axis',(0.,0.,-1.));
#16530=DIRECTION('',(-1.,0.,0.));
#16531=DIRECTION('center_axis',(-1.,0.,0.));
#16532=DIRECTION('ref_axis',(0.,0.,-1.));
#16533=DIRECTION('center_axis',(1.,0.,0.));
#16534=DIRECTION('ref_axis',(0.,0.,-1.));
#20616=CARTESIAN_POINT('',(0.,0.,0.));
#20617=CARTESIAN_POINT('Origin',(-0.3,-4.5,9.85));
#20618=CARTESIAN_POINT('',(-0.2,-4.5,10.075));
#20619=CARTESIAN_POINT('Origin',(-0.2,-4.5,9.85));
#20620=CARTESIAN_POINT('',(0.,-4.5,10.075));
#20621=CARTESIAN_POINT('',(-0.3,-4.5,10.075));
#20622=CARTESIAN_POINT('Origin',(0.,-4.5,9.85));
#20623=CARTESIAN_POINT('Origin',(-0.3,-4.5,6.15));
#20624=CARTESIAN_POINT('',(-0.2,-4.5,6.375));
#20625=CARTESIAN_POINT('Origin',(-0.2,-4.5,6.15));
#20626=CARTESIAN_POINT('',(0.,-4.5,6.375));
#20627=CARTESIAN_POINT('',(-0.3,-4.5,6.375));
#20628=CARTESIAN_POINT('Origin',(0.,-4.5,6.15));
#20629=CARTESIAN_POINT('Origin',(-0.3,-7.,8.));
#20630=CARTESIAN_POINT('',(0.,-6.55758,7.58004221212127));
#20631=CARTESIAN_POINT('',(-0.2,-6.55758,7.58004221212127));
#20632=CARTESIAN_POINT('',(-0.3,-6.55758,7.58004221212127));
#20633=CARTESIAN_POINT('',(0.,-6.55758,8.41995778787873));
#20634=CARTESIAN_POINT('Origin',(0.,-7.,8.));
#20635=CARTESIAN_POINT('',(-0.2,-6.55758,8.41995778787873));
#20636=CARTESIAN_POINT('',(-0.3,-6.55758,8.41995778787873));
#20637=CARTESIAN_POINT('Origin',(-0.2,-7.,8.));
#20638=CARTESIAN_POINT('Origin',(-0.3,-2.,8.));
#20639=CARTESIAN_POINT('',(0.,-2.44242,8.41995778787873));
#20640=CARTESIAN_POINT('',(-0.2,-2.44242,8.41995778787873));
#20641=CARTESIAN_POINT('',(-0.3,-2.44242,8.41995778787873));
#20642=CARTESIAN_POINT('',(0.,-2.44242,7.58004221212127));
#20643=CARTESIAN_POINT('Origin',(0.,-2.,8.));
#20644=CARTESIAN_POINT('',(-0.2,-2.44242,7.58004221212127));
#20645=CARTESIAN_POINT('',(-0.3,-2.44242,7.58004221212127));
#20646=CARTESIAN_POINT('Origin',(-0.2,-2.,8.));
#20647=CARTESIAN_POINT('Origin',(0.,-4.5,8.));
#20648=CARTESIAN_POINT('Origin',(0.,-4.5,8.));
#20649=CARTESIAN_POINT('Origin',(0.,-4.5,8.));
#20650=CARTESIAN_POINT('',(0.,-4.5,9.02));
#20651=CARTESIAN_POINT('Origin',(0.,-4.5,8.));
#20652=CARTESIAN_POINT('Origin',(-0.2,-4.5,8.));
#20653=CARTESIAN_POINT('Origin',(-0.2,-4.5,8.));
#20654=CARTESIAN_POINT('Origin',(-0.2,-4.5,8.));
#20655=CARTESIAN_POINT('Origin',(-0.2,-4.5,8.));
#20656=CARTESIAN_POINT('Origin',(-0.2,-4.5,8.));
#20657=CARTESIAN_POINT('',(-0.2,-4.5,9.02));
#20658=CARTESIAN_POINT('',(-0.2,-4.5,9.02));
#20659=CARTESIAN_POINT('Origin',(-0.2,-4.5,8.));
#20660=CARTESIAN_POINT('Origin',(-0.2,-4.5,8.));
#23518=UNCERTAINTY_MEASURE_WITH_UNIT(LENGTH_MEASURE(0.001),#23729,
'DISTANCE_ACCURACY_VALUE',
'Maximum model space distance between geometric entities at asserted c
onnectivities');
#23611=UNCERTAINTY_MEASURE_WITH_UNIT(LENGTH_MEASURE(0.001),#23729,
'DISTANCE_ACCURACY_VALUE',
'Maximum model space distance between geometric entities at asserted c
onnectivities');
#23635=(
GEOMETRIC_REPRESENTATION_CONTEXT(3)
GLOBAL_UNCERTAINTY_ASSIGNED_CONTEXT((#23518))
GLOBAL_UNIT_ASSIGNED_CONTEXT((#23729,#23731,#23732))
REPRESENTATION_CONTEXT('','3D')
);
#23728=(
GEOMETRIC_REPRESENTATION_CONTEXT(3)
GLOBAL_UNCERTAINTY_ASSIGNED_CONTEXT((#23611))
GLOBAL_UNIT_ASSIGNED_CONTEXT((#23729,#23731,#23732))
REPRESENTATION_CONTEXT('','3D')
);
#23729=(
LENGTH_UNIT()
NAMED_UNIT(*)
SI_UNIT(.CENTI.,.METRE.)
);
#23731=(
NAMED_UNIT(*)
PLANE_ANGLE_UNIT()
SI_UNIT($,.RADIAN.)
);
#23732=(
NAMED_UNIT(*)
SI_UNIT($,.STERADIAN.)
SOLID_ANGLE_UNIT()
);
#23756=SHAPE_DEFINITION_REPRESENTATION(#23872,#24135);
#23872=PRODUCT_DEFINITION_SHAPE('',$,#24252);
#24135=SHAPE_REPRESENTATION('',(#14075),#23635);
#24228=PRODUCT_DEFINITION_CONTEXT('part definition',#24578,'design');
#24252=PRODUCT_DEFINITION('Screw bearing keeper (2)',
'Screw bearing keeper (2)',#24368,#24228);
#24368=PRODUCT_DEFINITION_FORMATION('',$,#24603);
#24578=APPLICATION_CONTEXT(
'Core Data for Automotive Mechanical Design Process');
#24579=PRODUCT_CONTEXT('part definition',#24578,'mechanical');
#24603=PRODUCT('Screw bearing keeper (2)','Screw bearing keeper (2)',
'Screw bearing keeper (2)',(#24579));
#24766=COLOUR_RGB('Black',0.12,0.14,0.17);
#24767=FILL_AREA_STYLE_COLOUR('',#24766);
#24768=FILL_AREA_STYLE('',(#24767));
#24769=SURFACE_STYLE_FILL_AREA(#24768);
#24770=SURFACE_SIDE_STYLE('',(#24769));
#24771=SURFACE_STYLE_USAGE(.BOTH.,#24770);
#24772=PRESENTATION_STYLE_ASSIGNMENT((#24771));
ENDSEC;
END-ISO-10303-21;
